ISO-10303-21;
HEADER;
/* Generated by software containing ST-Developer
 * from STEP Tools, Inc. (www.steptools.com) 
 */

FILE_DESCRIPTION(
/* description */ ('Self-centering screw clamp'),
/* implementation_level */ '2;1');

FILE_NAME(
/* name */ 'Cap Screw - M4x16.step',
/* time_stamp */ '2026-10-28T03:25:31-07:00',
/* author */ (''),
/* organization */ (''),
/* preprocessor_version */ 'ST-DEVELOPER v20.2',
/* originating_system */ 'Autodesk Translation Framework v15.17.0.0',
/* authorisation */ '');

FILE_SCHEMA (('AUTOMOTIVE_DESIGN { 1 0 10303 214 3 1 1 }'));
ENDSEC;

DATA;
#10=MECHANICAL_DESIGN_GEOMETRIC_PRESENTATION_REPRESENTATION('',(#670),#16799);
#12=ORIENTED_CLOSED_SHELL('',*,#9123,.F.);
#14=BREP_WITH_VOIDS('Body1',#9122,(#12));
#492=CONICAL_SURFACE('',#10606,0.325,0.785398163397448);
#493=CONICAL_SURFACE('',#10610,0.335,0.785398163397448);
#494=CONICAL_SURFACE('',#10614,0.21,0.463647609000806);
#495=CONICAL_SURFACE('',#10618,0.18,0.785398163397448);
#581=SHAPE_REPRESENTATION_RELATIONSHIP('SRR','None',#17059,#622);
#622=ADVANCED_BREP_SHAPE_REPRESENTATION('',(#14),#16797);
#670=STYLED_ITEM('',(#17333),#14);
#1012=FACE_BOUND('',#2551,.T.);
#1253=PLANE('',#10604);
#1254=PLANE('',#10612);
#1255=PLANE('',#10620);
#1256=PLANE('',#10621);
#1257=PLANE('',#10622);
#1258=PLANE('',#10623);
#1259=PLANE('',#10624);
#1260=PLANE('',#10625);
#1261=PLANE('',#10626);
#1262=PLANE('',#10627);
#1263=PLANE('',#10628);
#1748=FACE_OUTER_BOUND('',#2546,.T.);
#1749=FACE_OUTER_BOUND('',#2547,.T.);
#1750=FACE_OUTER_BOUND('',#2548,.T.);
#1751=FACE_OUTER_BOUND('',#2549,.T.);
#1752=FACE_OUTER_BOUND('',#2550,.T.);
#1753=FACE_OUTER_BOUND('',#2552,.T.);
#1754=FACE_OUTER_BOUND('',#2553,.T.);
#1755=FACE_OUTER_BOUND('',#2554,.T.);
#1756=FACE_OUTER_BOUND('',#2555,.T.);
#1757=FACE_OUTER_BOUND('',#2556,.T.);
#1758=FACE_OUTER_BOUND('',#2557,.T.);
#1759=FACE_OUTER_BOUND('',#2558,.T.);
#1760=FACE_OUTER_BOUND('',#2559,.T.);
#1761=FACE_OUTER_BOUND('',#2560,.T.);
#1762=FACE_OUTER_BOUND('',#2561,.T.);
#1763=FACE_OUTER_BOUND('',#2562,.T.);
#1764=FACE_OUTER_BOUND('',#2563,.T.);
#2546=EDGE_LOOP('',(#8243));
#2547=EDGE_LOOP('',(#8244,#8245,#8246,#8247));
#2548=EDGE_LOOP('',(#8248,#8249,#8250,#8251));
#2549=EDGE_LOOP('',(#8252,#8253,#8254,#8255));
#2550=EDGE_LOOP('',(#8256));
#2551=EDGE_LOOP('',(#8257));
#2552=EDGE_LOOP('',(#8258,#8259,#8260,#8261));
#2553=EDGE_LOOP('',(#8262,#8263,#8264,#8265));
#2554=EDGE_LOOP('',(#8266,#8267,#8268,#8269));
#2555=EDGE_LOOP('',(#8270));
#2556=EDGE_LOOP('',(#8271,#8272,#8273,#8274));
#2557=EDGE_LOOP('',(#8275,#8276,#8277,#8278));
#2558=EDGE_LOOP('',(#8279,#8280,#8281,#8282));
#2559=EDGE_LOOP('',(#8283,#8284,#8285,#8286));
#2560=EDGE_LOOP('',(#8287,#8288,#8289,#8290));
#2561=EDGE_LOOP('',(#8291,#8292,#8293,#8294));
#2562=EDGE_LOOP('',(#8295,#8296,#8297,#8298,#8299,#8300));
#2563=EDGE_LOOP('',(#8301,#8302,#8303,#8304,#8305,#8306));
#3105=LINE('',#16479,#3678);
#3106=LINE('',#16483,#3679);
#3107=LINE('',#16487,#3680);
#3108=LINE('',#16494,#3681);
#3109=LINE('',#16498,#3682);
#3110=LINE('',#16502,#3683);
#3111=LINE('',#16507,#3684);
#3112=LINE('',#16509,#3685);
#3113=LINE('',#16511,#3686);
#3114=LINE('',#16512,#3687);
#3115=LINE('',#16515,#3688);
#3116=LINE('',#16517,#3689);
#3117=LINE('',#16518,#3690);
#3118=LINE('',#16521,#3691);
#3119=LINE('',#16523,#3692);
#3120=LINE('',#16524,#3693);
#3121=LINE('',#16527,#3694);
#3122=LINE('',#16529,#3695);
#3123=LINE('',#16530,#3696);
#3124=LINE('',#16533,#3697);
#3125=LINE('',#16535,#3698);
#3126=LINE('',#16536,#3699);
#3127=LINE('',#16538,#3700);
#3128=LINE('',#16539,#3701);
#3678=VECTOR('',#13342,0.325);
#3679=VECTOR('',#13347,0.35);
#3680=VECTOR('',#13352,0.335);
#3681=VECTOR('',#13361,0.21);
#3682=VECTOR('',#13366,0.2);
#3683=VECTOR('',#13371,0.18);
#3684=VECTOR('',#13376,1.);
#3685=VECTOR('',#13377,1.);
#3686=VECTOR('',#13378,1.);
#3687=VECTOR('',#13379,1.);
#3688=VECTOR('',#13382,1.);
#3689=VECTOR('',#13383,1.);
#3690=VECTOR('',#13384,1.);
#3691=VECTOR('',#13387,1.);
#3692=VECTOR('',#13388,1.);
#3693=VECTOR('',#13389,1.);
#3694=VECTOR('',#13392,1.);
#3695=VECTOR('',#13393,1.);
#3696=VECTOR('',#13394,1.);
#3697=VECTOR('',#13397,1.);
#3698=VECTOR('',#13398,1.);
#3699=VECTOR('',#13399,1.);
#3700=VECTOR('',#13402,1.);
#3701=VECTOR('',#13403,1.);
#4221=CIRCLE('',#10605,0.3);
#4222=CIRCLE('',#10607,0.35);
#4223=CIRCLE('',#10609,0.35);
#4224=CIRCLE('',#10611,0.32);
#4225=CIRCLE('',#10613,0.22);
#4226=CIRCLE('',#10615,0.1954);
#4227=CIRCLE('',#10617,0.1954);
#4228=CIRCLE('',#10619,0.16);
#4940=VERTEX_POINT('',#16474);
#4941=VERTEX_POINT('',#16477);
#4942=VERTEX_POINT('',#16481);
#4943=VERTEX_POINT('',#16485);
#4944=VERTEX_POINT('',#16489);
#4945=VERTEX_POINT('',#16492);
#4946=VERTEX_POINT('',#16496);
#4947=VERTEX_POINT('',#16500);
#4948=VERTEX_POINT('',#16505);
#4949=VERTEX_POINT('',#16506);
#4950=VERTEX_POINT('',#16508);
#4951=VERTEX_POINT('',#16510);
#4952=VERTEX_POINT('',#16514);
#4953=VERTEX_POINT('',#16516);
#4954=VERTEX_POINT('',#16520);
#4955=VERTEX_POINT('',#16522);
#4956=VERTEX_POINT('',#16526);
#4957=VERTEX_POINT('',#16528);
#4958=VERTEX_POINT('',#16532);
#4959=VERTEX_POINT('',#16534);
#6046=EDGE_CURVE('',#4940,#4940,#4221,.T.);
#6047=EDGE_CURVE('',#4941,#4941,#4222,.T.);
#6048=EDGE_CURVE('',#4941,#4940,#3105,.T.);
#6049=EDGE_CURVE('',#4942,#4942,#4223,.T.);
#6050=EDGE_CURVE('',#4942,#4941,#3106,.T.);
#6051=EDGE_CURVE('',#4943,#4943,#4224,.T.);
#6052=EDGE_CURVE('',#4943,#4942,#3107,.T.);
#6053=EDGE_CURVE('',#4944,#4944,#4225,.T.);
#6054=EDGE_CURVE('',#4945,#4945,#4226,.F.);
#6055=EDGE_CURVE('',#4945,#4944,#3108,.T.);
#6056=EDGE_CURVE('',#4946,#4946,#4227,.F.);
#6057=EDGE_CURVE('',#4946,#4945,#3109,.T.);
#6058=EDGE_CURVE('',#4947,#4947,#4228,.T.);
#6059=EDGE_CURVE('',#4947,#4946,#3110,.T.);
#6060=EDGE_CURVE('',#4948,#4949,#3111,.T.);
#6061=EDGE_CURVE('',#4949,#4950,#3112,.T.);
#6062=EDGE_CURVE('',#4950,#4951,#3113,.T.);
#6063=EDGE_CURVE('',#4948,#4951,#3114,.T.);
#6064=EDGE_CURVE('',#4949,#4952,#3115,.T.);
#6065=EDGE_CURVE('',#4952,#4953,#3116,.T.);
#6066=EDGE_CURVE('',#4953,#4950,#3117,.T.);
#6067=EDGE_CURVE('',#4952,#4954,#3118,.T.);
#6068=EDGE_CURVE('',#4954,#4955,#3119,.T.);
#6069=EDGE_CURVE('',#4955,#4953,#3120,.T.);
#6070=EDGE_CURVE('',#4954,#4956,#3121,.T.);
#6071=EDGE_CURVE('',#4956,#4957,#3122,.T.);
#6072=EDGE_CURVE('',#4957,#4955,#3123,.T.);
#6073=EDGE_CURVE('',#4956,#4958,#3124,.T.);
#6074=EDGE_CURVE('',#4958,#4959,#3125,.T.);
#6075=EDGE_CURVE('',#4959,#4957,#3126,.T.);
#6076=EDGE_CURVE('',#4958,#4948,#3127,.T.);
#6077=EDGE_CURVE('',#4951,#4959,#3128,.T.);
#8243=ORIENTED_EDGE('',*,*,#6046,.F.);
#8244=ORIENTED_EDGE('',*,*,#6047,.F.);
#8245=ORIENTED_EDGE('',*,*,#6048,.T.);
#8246=ORIENTED_EDGE('',*,*,#6046,.T.);
#8247=ORIENTED_EDGE('',*,*,#6048,.F.);
#8248=ORIENTED_EDGE('',*,*,#6049,.F.);
#8249=ORIENTED_EDGE('',*,*,#6050,.T.);
#8250=ORIENTED_EDGE('',*,*,#6047,.T.);
#8251=ORIENTED_EDGE('',*,*,#6050,.F.);
#8252=ORIENTED_EDGE('',*,*,#6051,.F.);
#8253=ORIENTED_EDGE('',*,*,#6052,.T.);
#8254=ORIENTED_EDGE('',*,*,#6049,.T.);
#8255=ORIENTED_EDGE('',*,*,#6052,.F.);
#8256=ORIENTED_EDGE('',*,*,#6051,.T.);
#8257=ORIENTED_EDGE('',*,*,#6053,.F.);
#8258=ORIENTED_EDGE('',*,*,#6054,.F.);
#8259=ORIENTED_EDGE('',*,*,#6055,.T.);
#8260=ORIENTED_EDGE('',*,*,#6053,.T.);
#8261=ORIENTED_EDGE('',*,*,#6055,.F.);
#8262=ORIENTED_EDGE('',*,*,#6056,.F.);
#8263=ORIENTED_EDGE('',*,*,#6057,.T.);
#8264=ORIENTED_EDGE('',*,*,#6054,.T.);
#8265=ORIENTED_EDGE('',*,*,#6057,.F.);
#8266=ORIENTED_EDGE('',*,*,#6058,.F.);
#8267=ORIENTED_EDGE('',*,*,#6059,.T.);
#8268=ORIENTED_EDGE('',*,*,#6056,.T.);
#8269=ORIENTED_EDGE('',*,*,#6059,.F.);
#8270=ORIENTED_EDGE('',*,*,#6058,.T.);
#8271=ORIENTED_EDGE('',*,*,#6060,.T.);
#8272=ORIENTED_EDGE('',*,*,#6061,.T.);
#8273=ORIENTED_EDGE('',*,*,#6062,.T.);
#8274=ORIENTED_EDGE('',*,*,#6063,.F.);
#8275=ORIENTED_EDGE('',*,*,#6064,.T.);
#8276=ORIENTED_EDGE('',*,*,#6065,.T.);
#8277=ORIENTED_EDGE('',*,*,#6066,.T.);
#8278=ORIENTED_EDGE('',*,*,#6061,.F.);
#8279=ORIENTED_EDGE('',*,*,#6067,.T.);
#8280=ORIENTED_EDGE('',*,*,#6068,.T.);
#8281=ORIENTED_EDGE('',*,*,#6069,.T.);
#8282=ORIENTED_EDGE('',*,*,#6065,.F.);
#8283=ORIENTED_EDGE('',*,*,#6070,.T.);
#8284=ORIENTED_EDGE('',*,*,#6071,.T.);
#8285=ORIENTED_EDGE('',*,*,#6072,.T.);
#8286=ORIENTED_EDGE('',*,*,#6068,.F.);
#8287=ORIENTED_EDGE('',*,*,#6073,.T.);
#8288=ORIENTED_EDGE('',*,*,#6074,.T.);
#8289=ORIENTED_EDGE('',*,*,#6075,.T.);
#8290=ORIENTED_EDGE('',*,*,#6071,.F.);
#8291=ORIENTED_EDGE('',*,*,#6076,.T.);
#8292=ORIENTED_EDGE('',*,*,#6063,.T.);
#8293=ORIENTED_EDGE('',*,*,#6077,.T.);
#8294=ORIENTED_EDGE('',*,*,#6074,.F.);
#8295=ORIENTED_EDGE('',*,*,#6076,.F.);
#8296=ORIENTED_EDGE('',*,*,#6073,.F.);
#8297=ORIENTED_EDGE('',*,*,#6070,.F.);
#8298=ORIENTED_EDGE('',*,*,#6067,.F.);
#8299=ORIENTED_EDGE('',*,*,#6064,.F.);
#8300=ORIENTED_EDGE('',*,*,#6060,.F.);
#8301=ORIENTED_EDGE('',*,*,#6077,.F.);
#8302=ORIENTED_EDGE('',*,*,#6062,.F.);
#8303=ORIENTED_EDGE('',*,*,#6066,.F.);
#8304=ORIENTED_EDGE('',*,*,#6069,.F.);
#8305=ORIENTED_EDGE('',*,*,#6072,.F.);
#8306=ORIENTED_EDGE('',*,*,#6075,.F.);
#8568=CYLINDRICAL_SURFACE('',#10608,0.35);
#8569=CYLINDRICAL_SURFACE('',#10616,0.1954);
#9046=ADVANCED_FACE('',(#1748),#1253,.T.);
#9047=ADVANCED_FACE('',(#1749),#492,.T.);
#9048=ADVANCED_FACE('',(#1750),#8568,.T.);
#9049=ADVANCED_FACE('',(#1751),#493,.T.);
#9050=ADVANCED_FACE('',(#1752,#1012),#1254,.T.);
#9051=ADVANCED_FACE('',(#1753),#494,.T.);
#9052=ADVANCED_FACE('',(#1754),#8569,.T.);
#9053=ADVANCED_FACE('',(#1755),#495,.T.);
#9054=ADVANCED_FACE('',(#1756),#1255,.T.);
#9055=ADVANCED_FACE('',(#1757),#1256,.F.);
#9056=ADVANCED_FACE('',(#1758),#1257,.F.);
#9057=ADVANCED_FACE('',(#1759),#1258,.F.);
#9058=ADVANCED_FACE('',(#1760),#1259,.F.);
#9059=ADVANCED_FACE('',(#1761),#1260,.F.);
#9060=ADVANCED_FACE('',(#1762),#1261,.F.);
#9061=ADVANCED_FACE('',(#1763),#1262,.F.);
#9062=ADVANCED_FACE('',(#1764),#1263,.F.);
#9122=CLOSED_SHELL('',(#9046,#9047,#9048,#9049,#9050,#9051,#9052,#9053,
#9054));
#9123=CLOSED_SHELL('',(#9055,#9056,#9057,#9058,#9059,#9060,#9061,#9062));
#10603=AXIS2_PLACEMENT_3D('',#16472,#13332,#13333);
#10604=AXIS2_PLACEMENT_3D('',#16473,#13334,#13335);
#10605=AXIS2_PLACEMENT_3D('',#16475,#13336,#13337);
#10606=AXIS2_PLACEMENT_3D('',#16476,#13338,#13339);
#10607=AXIS2_PLACEMENT_3D('',#16478,#13340,#13341);
#10608=AXIS2_PLACEMENT_3D('',#16480,#13343,#13344);
#10609=AXIS2_PLACEMENT_3D('',#16482,#13345,#13346);
#10610=AXIS2_PLACEMENT_3D('',#16484,#13348,#13349);
#10611=AXIS2_PLACEMENT_3D('',#16486,#13350,#13351);
#10612=AXIS2_PLACEMENT_3D('',#16488,#13353,#13354);
#10613=AXIS2_PLACEMENT_3D('',#16490,#13355,#13356);
#10614=AXIS2_PLACEMENT_3D('',#16491,#13357,#13358);
#10615=AXIS2_PLACEMENT_3D('',#16493,#13359,#13360);
#10616=AXIS2_PLACEMENT_3D('',#16495,#13362,#13363);
#10617=AXIS2_PLACEMENT_3D('',#16497,#13364,#13365);
#10618=AXIS2_PLACEMENT_3D('',#16499,#13367,#13368);
#10619=AXIS2_PLACEMENT_3D('',#16501,#13369,#13370);
#10620=AXIS2_PLACEMENT_3D('',#16503,#13372,#13373);
#10621=AXIS2_PLACEMENT_3D('',#16504,#13374,#13375);
#10622=AXIS2_PLACEMENT_3D('',#16513,#13380,#13381);
#10623=AXIS2_PLACEMENT_3D('',#16519,#13385,#13386);
#10624=AXIS2_PLACEMENT_3D('',#16525,#13390,#13391);
#10625=AXIS2_PLACEMENT_3D('',#16531,#13395,#13396);
#10626=AXIS2_PLACEMENT_3D('',#16537,#13400,#13401);
#10627=AXIS2_PLACEMENT_3D('',#16540,#13404,#13405);
#10628=AXIS2_PLACEMENT_3D('',#16541,#13406,#13407);
#13332=DIRECTION('axis',(0.,0.,1.));
#13333=DIRECTION('refdir',(1.,0.,0.));
#13334=DIRECTION('center_axis',(0.,1.,0.));
#13335=DIRECTION('ref_axis',(0.,0.,1.));
#13336=DIRECTION('center_axis',(0.,-1.,0.));
#13337=DIRECTION('ref_axis',(1.,0.,0.));
#13338=DIRECTION('center_axis',(0.,-1.,0.));
#13339=DIRECTION('ref_axis',(1.,0.,0.));
#13340=DIRECTION('center_axis',(0.,-1.,0.));
#13341=DIRECTION('ref_axis',(1.,0.,0.));
#13342=DIRECTION('',(0.707106781186547,0.707106781186548,8.65956056235493E-17));
#13343=DIRECTION('center_axis',(0.,-1.,0.));
#13344=DIRECTION('ref_axis',(1.,0.,0.));
#13345=DIRECTION('center_axis',(0.,-1.,0.));
#13346=DIRECTION('ref_axis',(1.,0.,0.));
#13347=DIRECTION('',(0.,1.,0.));
#13348=DIRECTION('center_axis',(0.,1.,0.));
#13349=DIRECTION('ref_axis',(1.,0.,0.));
#13350=DIRECTION('center_axis',(0.,-1.,0.));
#13351=DIRECTION('ref_axis',(1.,0.,0.));
#13352=DIRECTION('',(-0.707106781186547,0.707106781186548,-8.65956056235493E-17));
#13353=DIRECTION('center_axis',(0.,-1.,0.));
#13354=DIRECTION('ref_axis',(0.,0.,-1.));
#13355=DIRECTION('center_axis',(0.,-1.,0.));
#13356=DIRECTION('ref_axis',(1.,0.,0.));
#13357=DIRECTION('center_axis',(0.,1.,0.));
#13358=DIRECTION('ref_axis',(1.,0.,0.));
#13359=DIRECTION('center_axis',(0.,1.,0.));
#13360=DIRECTION('ref_axis',(1.,0.,0.));
#13361=DIRECTION('',(-0.447213595499958,0.894427190999916,-5.47678698264203E-17));
#13362=DIRECTION('center_axis',(0.,-1.,0.));
#13363=DIRECTION('ref_axis',(1.,0.,0.));
#13364=DIRECTION('center_axis',(0.,1.,0.));
#13365=DIRECTION('ref_axis',(1.,0.,0.));
#13366=DIRECTION('',(0.,1.,0.));
#13367=DIRECTION('center_axis',(0.,1.,0.));
#13368=DIRECTION('ref_axis',(1.,0.,0.));
#13369=DIRECTION('center_axis',(0.,-1.,0.));
#13370=DIRECTION('ref_axis',(1.,0.,0.));
#13371=DIRECTION('',(-0.707106781186547,0.707106781186548,-8.65956056235493E-17));
#13372=DIRECTION('center_axis',(0.,-1.,0.));
#13373=DIRECTION('ref_axis',(0.,0.,-1.));
#13374=DIRECTION('center_axis',(0.866025403784439,0.,-0.5));
#13375=DIRECTION('ref_axis',(0.5,0.,0.866025403784439));
#13376=DIRECTION('',(-0.5,0.,-0.866025403784439));
#13377=DIRECTION('',(0.,-1.,0.));
#13378=DIRECTION('',(0.5,0.,0.866025403784439));
#13379=DIRECTION('',(0.,-1.,0.));
#13380=DIRECTION('center_axis',(1.60246890531964E-16,0.,-1.));
#13381=DIRECTION('ref_axis',(1.,0.,1.60246890531964E-16));
#13382=DIRECTION('',(-1.,0.,-1.60246890531964E-16));
#13383=DIRECTION('',(0.,-1.,0.));
#13384=DIRECTION('',(1.,0.,1.60246890531964E-16));
#13385=DIRECTION('center_axis',(-0.866025403784439,0.,-0.5));
#13386=DIRECTION('ref_axis',(0.5,0.,-0.866025403784439));
#13387=DIRECTION('',(-0.5,0.,0.866025403784439));
#13388=DIRECTION('',(0.,-1.,0.));
#13389=DIRECTION('',(0.5,0.,-0.866025403784439));
#13390=DIRECTION('center_axis',(-0.866025403784439,0.,0.5));
#13391=DIRECTION('ref_axis',(-0.5,0.,-0.866025403784439));
#13392=DIRECTION('',(0.5,0.,0.866025403784439));
#13393=DIRECTION('',(0.,-1.,0.));
#13394=DIRECTION('',(-0.5,0.,-0.866025403784439));
#13395=DIRECTION('center_axis',(-1.60246890531964E-16,0.,1.));
#13396=DIRECTION('ref_axis',(-1.,0.,-1.60246890531964E-16));
#13397=DIRECTION('',(1.,0.,1.60246890531964E-16));
#13398=DIRECTION('',(0.,-1.,0.));
#13399=DIRECTION('',(-1.,0.,-1.60246890531964E-16));
#13400=DIRECTION('center_axis',(0.866025403784439,0.,0.5));
#13401=DIRECTION('ref_axis',(-0.5,0.,0.866025403784439));
#13402=DIRECTION('',(0.5,0.,-0.866025403784439));
#13403=DIRECTION('',(-0.5,0.,0.866025403784439));
#13404=DIRECTION('center_axis',(0.,1.,0.));
#13405=DIRECTION('ref_axis',(1.,0.,0.));
#13406=DIRECTION('center_axis',(0.,-1.,0.));
#13407=DIRECTION('ref_axis',(0.,0.,-1.));
#16472=CARTESIAN_POINT('',(0.,0.,0.));
#16473=CARTESIAN_POINT('Origin',(0.3,0.4,0.));
#16474=CARTESIAN_POINT('',(-0.3,0.4,-3.67394039744206E-17));
#16475=CARTESIAN_POINT('Origin',(0.,0.4,0.));
#16476=CARTESIAN_POINT('Origin',(0.,0.375,0.));
#16477=CARTESIAN_POINT('',(-0.35,0.35,-4.28626379701573E-17));
#16478=CARTESIAN_POINT('Origin',(0.,0.35,0.));
#16479=CARTESIAN_POINT('',(-0.325,0.375,-3.9801020972289E-17));
#16480=CARTESIAN_POINT('Origin',(0.,0.19,0.));
#16481=CARTESIAN_POINT('',(-0.35,0.03,-4.28626379701574E-17));
#16482=CARTESIAN_POINT('Origin',(0.,0.03,0.));
#16483=CARTESIAN_POINT('',(-0.35,0.19,-4.28626379701574E-17));
#16484=CARTESIAN_POINT('Origin',(0.,0.0149999999999999,0.));
#16485=CARTESIAN_POINT('',(-0.32,-3.29597460435593E-17,-3.91886975727153E-17));
#16486=CARTESIAN_POINT('Origin',(0.,0.,0.));
#16487=CARTESIAN_POINT('',(-0.335,0.0149999999999999,-4.10256677714363E-17));
#16488=CARTESIAN_POINT('Origin',(0.22,0.,0.));
#16489=CARTESIAN_POINT('',(-0.22,-6.93889390390723E-18,-2.69422295812418E-17));
#16490=CARTESIAN_POINT('Origin',(0.,0.,0.));
#16491=CARTESIAN_POINT('Origin',(0.,-0.02,0.));
#16492=CARTESIAN_POINT('',(-0.1954,-0.0492,2.39295984553393E-17));
#16493=CARTESIAN_POINT('Origin',(0.,-0.0492,0.));
#16494=CARTESIAN_POINT('',(-0.21,-0.02,-2.57175827820944E-17));
#16495=CARTESIAN_POINT('Origin',(0.,-0.8,0.));
#16496=CARTESIAN_POINT('',(-0.1954,-1.5646,2.39295984553393E-17));
#16497=CARTESIAN_POINT('Origin',(0.,-1.5646,0.));
#16498=CARTESIAN_POINT('',(-0.1954,-0.8,-2.39295984553393E-17));
#16499=CARTESIAN_POINT('Origin',(0.,-1.58,0.));
#16500=CARTESIAN_POINT('',(-0.16,-1.6,-1.95943487863577E-17));
#16501=CARTESIAN_POINT('Origin',(0.,-1.6,0.));
#16502=CARTESIAN_POINT('',(-0.18,-1.58,-2.20436423846524E-17));
#16503=CARTESIAN_POINT('Origin',(0.,-1.6,0.));
#16504=CARTESIAN_POINT('Origin',(0.0866025403784439,-0.4,-0.15));
#16505=CARTESIAN_POINT('',(0.173205080756888,-0.4,0.));
#16506=CARTESIAN_POINT('',(0.0866025403784439,-0.4,-0.15));
#16507=CARTESIAN_POINT('',(0.173205080756888,-0.4,0.));
#16508=CARTESIAN_POINT('',(0.0866025403784439,-0.64,-0.15));
#16509=CARTESIAN_POINT('',(0.0866025403784439,-0.4,-0.15));
#16510=CARTESIAN_POINT('',(0.173205080756888,-0.64,0.));
#16511=CARTESIAN_POINT('',(0.173205080756888,-0.64,0.));
#16512=CARTESIAN_POINT('',(0.173205080756888,-0.4,0.));
#16513=CARTESIAN_POINT('Origin',(-0.0866025403784438,-0.4,-0.15));
#16514=CARTESIAN_POINT('',(-0.0866025403784438,-0.4,-0.15));
#16515=CARTESIAN_POINT('',(0.0866025403784439,-0.4,-0.15));
#16516=CARTESIAN_POINT('',(-0.0866025403784438,-0.64,-0.15));
#16517=CARTESIAN_POINT('',(-0.0866025403784438,-0.4,-0.15));
#16518=CARTESIAN_POINT('',(0.0866025403784439,-0.64,-0.15));
#16519=CARTESIAN_POINT('Origin',(-0.173205080756888,-0.4,-2.77555756156289E-17));
#16520=CARTESIAN_POINT('',(-0.173205080756888,-0.4,-2.12115047744981E-17));
#16521=CARTESIAN_POINT('',(-0.0866025403784438,-0.4,-0.15));
#16522=CARTESIAN_POINT('',(-0.173205080756888,-0.64,-2.77555756156289E-17));
#16523=CARTESIAN_POINT('',(-0.173205080756888,-0.4,-2.12115047744981E-17));
#16524=CARTESIAN_POINT('',(-0.0866025403784438,-0.64,-0.15));
#16525=CARTESIAN_POINT('Origin',(-0.0866025403784439,-0.4,0.15));
#16526=CARTESIAN_POINT('',(-0.0866025403784439,-0.4,0.15));
#16527=CARTESIAN_POINT('',(-0.173205080756888,-0.4,-2.12115047744981E-17));
#16528=CARTESIAN_POINT('',(-0.0866025403784439,-0.64,0.15));
#16529=CARTESIAN_POINT('',(-0.0866025403784439,-0.4,0.15));
#16530=CARTESIAN_POINT('',(-0.173205080756888,-0.64,-2.12115047744981E-17));
#16531=CARTESIAN_POINT('Origin',(0.0866025403784439,-0.4,0.15));
#16532=CARTESIAN_POINT('',(0.0866025403784439,-0.4,0.15));
#16533=CARTESIAN_POINT('',(-0.0866025403784439,-0.4,0.15));
#16534=CARTESIAN_POINT('',(0.0866025403784439,-0.64,0.15));
#16535=CARTESIAN_POINT('',(0.0866025403784439,-0.4,0.15));
#16536=CARTESIAN_POINT('',(-0.0866025403784439,-0.64,0.15));
#16537=CARTESIAN_POINT('Origin',(0.173205080756888,-0.4,0.));
#16538=CARTESIAN_POINT('',(0.0866025403784439,-0.4,0.15));
#16539=CARTESIAN_POINT('',(0.0866025403784439,-0.64,0.15));
#16540=CARTESIAN_POINT('Origin',(0.,-0.4,-2.77555756156289E-17));
#16541=CARTESIAN_POINT('Origin',(0.,-0.64,-2.77555756156289E-17));
#16748=UNCERTAINTY_MEASURE_WITH_UNIT(LENGTH_MEASURE(0.001),#16800,
'DISTANCE_ACCURACY_VALUE',
'Maximum model space distance between geometric entities at asserted c
onnectivities');
#16750=UNCERTAINTY_MEASURE_WITH_UNIT(LENGTH_MEASURE(0.001),#16800,
'DISTANCE_ACCURACY_VALUE',
'Maximum model space distance between geometric entities at asserted c
onnectivities');
#16797=(
GEOMETRIC_REPRESENTATION_CONTEXT(3)
GLOBAL_UNCERTAINTY_ASSIGNED_CONTEXT((#16748))
GLOBAL_UNIT_ASSIGNED_CONTEXT((#16800,#16802,#16803))
REPRESENTATION_CONTEXT('','3D')
);
#16799=(
GEOMETRIC_REPRESENTATION_CONTEXT(3)
GLOBAL_UNCERTAINTY_ASSIGNED_CONTEXT((#16750))
GLOBAL_UNIT_ASSIGNED_CONTEXT((#16800,#16802,#16803))
REPRESENTATION_CONTEXT('','3D')
);
#16800=(
LENGTH_UNIT()
NAMED_UNIT(*)
SI_UNIT(.CENTI.,.METRE.)
);
#16802=(
NAMED_UNIT(*)
PLANE_ANGLE_UNIT()
SI_UNIT($,.RADIAN.)
);
#16803=(
NAMED_UNIT(*)
SI_UNIT($,.STERADIAN.)
SOLID_ANGLE_UNIT()
);
#16850=SHAPE_DEFINITION_REPRESENTATION(#16905,#17059);
#16905=PRODUCT_DEFINITION_SHAPE('',$,#17108);
#17059=SHAPE_REPRESENTATION('',(#10603),#16797);
#17061=PRODUCT_DEFINITION_CONTEXT('part definition',#17207,'design');
#17108=PRODUCT_DEFINITION('Cap Screw - M4x16','Cap Screw - M4x16',#17156,
#17061);
#17156=PRODUCT_DEFINITION_FORMATION('',$,#17255);
#17207=APPLICATION_CONTEXT(
'Core Data for Automotive Mechanical Design Process');
#17208=PRODUCT_CONTEXT('part definition',#17207,'mechanical');
#17255=PRODUCT('Cap Screw - M4x16','Cap Screw - M4x16',
'Cap Screw - M4x16',(#17208));
#17327=COLOUR_RGB('Black',0.12,0.14,0.17);
#17328=FILL_AREA_STYLE_COLOUR('',#17327);
#17329=FILL_AREA_STYLE('',(#17328));
#17330=SURFACE_STYLE_FILL_AREA(#17329);
#17331=SURFACE_SIDE_STYLE('',(#17330));
#17332=SURFACE_STYLE_USAGE(.BOTH.,#17331);
#17333=PRESENTATION_STYLE_ASSIGNMENT((#17332));
ENDSEC;
END-ISO-10303-21;
